ISO-10303-21;
HEADER;
/* Generated by software containing ST-Developer
 * from STEP Tools, Inc. (www.steptools.com) 
 */

FILE_DESCRIPTION(
/* description */ ('Jaw-coupled motor to shaft test stand'),
/* implementation_level */ '2;1');

FILE_NAME(
/* name */ 'Mounting reducer (3).step',
/* time_stamp */ '2026-10-27T10:46:06-07:00',
/* author */ (''),
/* organization */ (''),
/* preprocessor_version */ 'ST-DEVELOPER v20.2',
/* originating_system */ 'Autodesk Translation Framework v15.17.0.0',
/* authorisation */ '');

FILE_SCHEMA (('AUTOMOTIVE_DESIGN { 1 0 10303 214 3 1 1 }'));
ENDSEC;

DATA;
#10=MECHANICAL_DESIGN_GEOMETRIC_PRESENTATION_REPRESENTATION('',(#346),#19361);
#282=SHAPE_REPRESENTATION_RELATIONSHIP('SRR','None',#19496,#314);
#314=ADVANCED_BREP_SHAPE_REPRESENTATION('',(#379),#19332);
#346=STYLED_ITEM('',(#19739),#379);
#379=MANIFOLD_SOLID_BREP('Body1',#10990);
#421=FACE_BOUND('',#1699,.T.);
#422=FACE_BOUND('',#1701,.T.);
#540=PLANE('',#11448);
#541=PLANE('',#11449);
#1058=FACE_OUTER_BOUND('',#1696,.T.);
#1059=FACE_OUTER_BOUND('',#1697,.T.);
#1060=FACE_OUTER_BOUND('',#1698,.T.);
#1061=FACE_OUTER_BOUND('',#1700,.T.);
#1696=EDGE_LOOP('',(#7490,#7491,#7492,#7493));
#1697=EDGE_LOOP('',(#7494,#7495,#7496,#7497));
#1698=EDGE_LOOP('',(#7498));
#1699=EDGE_LOOP('',(#7499));
#1700=EDGE_LOOP('',(#7500));
#1701=EDGE_LOOP('',(#7501));
#2423=LINE('',#15596,#3576);
#2424=LINE('',#15602,#3577);
#3576=VECTOR('',#12530,0.425);
#3577=VECTOR('',#12537,0.645);
#4705=CIRCLE('',#11443,0.425);
#4706=CIRCLE('',#11444,0.425);
#4707=CIRCLE('',#11446,0.645);
#4708=CIRCLE('',#11447,0.645);
#4991=VERTEX_POINT('',#15593);
#4992=VERTEX_POINT('',#15595);
#4993=VERTEX_POINT('',#15599);
#4994=VERTEX_POINT('',#15601);
#5956=EDGE_CURVE('',#4991,#4991,#4705,.T.);
#5957=EDGE_CURVE('',#4991,#4992,#2423,.T.);
#5958=EDGE_CURVE('',#4992,#4992,#4706,.T.);
#5959=EDGE_CURVE('',#4993,#4993,#4707,.T.);
#5960=EDGE_CURVE('',#4993,#4994,#2424,.T.);
#5961=EDGE_CURVE('',#4994,#4994,#4708,.T.);
#7490=ORIENTED_EDGE('',*,*,#5956,.F.);
#7491=ORIENTED_EDGE('',*,*,#5957,.T.);
#7492=ORIENTED_EDGE('',*,*,#5958,.T.);
#7493=ORIENTED_EDGE('',*,*,#5957,.F.);
#7494=ORIENTED_EDGE('',*,*,#5959,.F.);
#7495=ORIENTED_EDGE('',*,*,#5960,.T.);
#7496=ORIENTED_EDGE('',*,*,#5961,.T.);
#7497=ORIENTED_EDGE('',*,*,#5960,.F.);
#7498=ORIENTED_EDGE('',*,*,#5959,.T.);
#7499=ORIENTED_EDGE('',*,*,#5956,.T.);
#7500=ORIENTED_EDGE('',*,*,#5961,.F.);
#7501=ORIENTED_EDGE('',*,*,#5958,.F.);
#10282=CYLINDRICAL_SURFACE('',#11442,0.425);
#10283=CYLINDRICAL_SURFACE('',#11445,0.645);
#10400=ADVANCED_FACE('',(#1058),#10282,.F.);
#10401=ADVANCED_FACE('',(#1059),#10283,.T.);
#10402=ADVANCED_FACE('',(#1060,#421),#540,.T.);
#10403=ADVANCED_FACE('',(#1061,#422),#541,.F.);
#10990=CLOSED_SHELL('',(#10400,#10401,#10402,#10403));
#11441=AXIS2_PLACEMENT_3D('',#15591,#12524,#12525);
#11442=AXIS2_PLACEMENT_3D('',#15592,#12526,#12527);
#11443=AXIS2_PLACEMENT_3D('',#15594,#12528,#12529);
#11444=AXIS2_PLACEMENT_3D('',#15597,#12531,#12532);
#11445=AXIS2_PLACEMENT_3D('',#15598,#12533,#12534);
#11446=AXIS2_PLACEMENT_3D('',#15600,#12535,#12536);
#11447=AXIS2_PLACEMENT_3D('',#15603,#12538,#12539);
#11448=AXIS2_PLACEMENT_3D('',#15604,#12540,#12541);
#11449=AXIS2_PLACEMENT_3D('',#15605,#12542,#12543);
#12524=DIRECTION('axis',(0.,0.,1.));
#12525=DIRECTION('refdir',(1.,0.,0.));
#12526=DIRECTION('center_axis',(0.,0.,1.));
#12527=DIRECTION('ref_axis',(1.,0.,0.));
#12528=DIRECTION('center_axis',(0.,0.,-1.));
#12529=DIRECTION('ref_axis',(1.,0.,0.));
#12530=DIRECTION('',(0.,0.,-1.));
#12531=DIRECTION('center_axis',(0.,0.,-1.));
#12532=DIRECTION('ref_axis',(1.,0.,0.));
#12533=DIRECTION('center_axis',(0.,0.,1.));
#12534=DIRECTION('ref_axis',(1.,0.,0.));
#12535=DIRECTION('center_axis',(0.,0.,1.));
#12536=DIRECTION('ref_axis',(1.,0.,0.));
#12537=DIRECTION('',(0.,0.,-1.));
#12538=DIRECTION('center_axis',(0.,0.,1.));
#12539=DIRECTION('ref_axis',(1.,0.,0.));
#12540=DIRECTION('center_axis',(0.,0.,1.));
#12541=DIRECTION('ref_axis',(1.,0.,0.));
#12542=DIRECTION('center_axis',(0.,0.,1.));
#12543=DIRECTION('ref_axis',(1.,0.,0.));
#15591=CARTESIAN_POINT('',(0.,0.,0.));
#15592=CARTESIAN_POINT('Origin',(4.75,18.,1.2));
#15593=CARTESIAN_POINT('',(4.325,18.,2.4));
#15594=CARTESIAN_POINT('Origin',(4.75,18.,2.4));
#15595=CARTESIAN_POINT('',(4.325,18.,1.2));
#15596=CARTESIAN_POINT('',(4.325,18.,1.2));
#15597=CARTESIAN_POINT('Origin',(4.75,18.,1.2));
#15598=CARTESIAN_POINT('Origin',(4.75,18.,1.2));
#15599=CARTESIAN_POINT('',(4.105,18.,2.4));
#15600=CARTESIAN_POINT('Origin',(4.75,18.,2.4));
#15601=CARTESIAN_POINT('',(4.105,18.,1.2));
#15602=CARTESIAN_POINT('',(4.105,18.,1.2));
#15603=CARTESIAN_POINT('Origin',(4.75,18.,1.2));
#15604=CARTESIAN_POINT('Origin',(4.75,18.,2.4));
#15605=CARTESIAN_POINT('Origin',(4.75,18.,1.2));
#19294=UNCERTAINTY_MEASURE_WITH_UNIT(LENGTH_MEASURE(0.001),#19362,
'DISTANCE_ACCURACY_VALUE',
'Maximum model space distance between geometric entities at asserted c
onnectivities');
#19323=UNCERTAINTY_MEASURE_WITH_UNIT(LENGTH_MEASURE(0.001),#19362,
'DISTANCE_ACCURACY_VALUE',
'Maximum model space distance between geometric entities at asserted c
onnectivities');
#19332=(
GEOMETRIC_REPRESENTATION_CONTEXT(3)
GLOBAL_UNCERTAINTY_ASSIGNED_CONTEXT((#19294))
GLOBAL_UNIT_ASSIGNED_CONTEXT((#19362,#19364,#19365))
REPRESENTATION_CONTEXT('','3D')
);
#19361=(
GEOMETRIC_REPRESENTATION_CONTEXT(3)
GLOBAL_UNCERTAINTY_ASSIGNED_CONTEXT((#19323))
GLOBAL_UNIT_ASSIGNED_CONTEXT((#19362,#19364,#19365))
REPRESENTATION_CONTEXT('','3D')
);
#19362=(
LENGTH_UNIT()
NAMED_UNIT(*)
SI_UNIT(.CENTI.,.METRE.)
);
#19364=(
NAMED_UNIT(*)
PLANE_ANGLE_UNIT()
SI_UNIT($,.RADIAN.)
);
#19365=(
NAMED_UNIT(*)
SI_UNIT($,.STERADIAN.)
SOLID_ANGLE_UNIT()
);
#19374=SHAPE_DEFINITION_REPRESENTATION(#19411,#19496);
#19411=PRODUCT_DEFINITION_SHAPE('',$,#19534);
#19496=SHAPE_REPRESENTATION('',(#11441),#19332);
#19525=PRODUCT_DEFINITION_CONTEXT('part definition',#19638,'design');
#19534=PRODUCT_DEFINITION('Mounting reducer (3)','Mounting reducer (3)',#19571,
#19525);
#19571=PRODUCT_DEFINITION_FORMATION('',$,#19648);
#19638=APPLICATION_CONTEXT(
'Core Data for Automotive Mechanical Design Process');
#19639=PRODUCT_CONTEXT('part definition',#19638,'mechanical');
#19648=PRODUCT('Mounting reducer (3)','Mounting reducer (3)',
'Mounting reducer (3)',(#19639));
#19733=COLOUR_RGB('Sky Blue',0.24,0.69,0.87);
#19734=FILL_AREA_STYLE_COLOUR('',#19733);
#19735=FILL_AREA_STYLE('',(#19734));
#19736=SURFACE_STYLE_FILL_AREA(#19735);
#19737=SURFACE_SIDE_STYLE('',(#19736));
#19738=SURFACE_STYLE_USAGE(.BOTH.,#19737);
#19739=PRESENTATION_STYLE_ASSIGNMENT((#19738));
ENDSEC;
END-ISO-10303-21;
